ISO-10303-21;
HEADER;
FILE_DESCRIPTION (('STEP AP214'),
    '1' );
FILE_NAME ('socket head cap screw_iso_ISO 4762 M10 x 70 - 32N.step',
    '2026-10-26T22:46:44',
    ( '' ),
    ( '' ),
    'SwSTEP 2.0',
    'SolidWorks 2025',
    '' );
FILE_SCHEMA (( 'AUTOMOTIVE_DESIGN' ));
ENDSEC;

DATA;
#4=DIRECTION ( 'NONE',  ( 0.000000000000000000, 0.4999999999999984457, -0.8660254037844395958 ) ) ;
#27=EDGE_CURVE ( 'NONE', #5527, #10122, #12164, .T. ) ;
#47=CIRCLE ( 'NONE', #14620, 8.000000000000058620 ) ;
#57=CARTESIAN_POINT ( 'NONE',  ( 80.00000000000000000, 0.000000000000000000, 0.000000000000000000 ) ) ;
#87=ORIENTED_EDGE ( 'NONE', *, *, #4132, .T. ) ;
#176=DIRECTION ( 'NONE',  ( 1.000000000000000000, 0.000000000000000000, 0.000000000000000000 ) ) ;
#182=CARTESIAN_POINT ( 'NONE',  ( 5.000000000000004441, -2.342598717236899830, 4.057500000000059615 ) ) ;
#203=ORIENTED_EDGE ( 'NONE', *, *, #13292, .F. ) ;
#218=EDGE_CURVE ( 'NONE', #14678, #19163, #6091, .T. ) ;
#220=ORIENTED_EDGE ( 'NONE', *, *, #3519, .T. ) ;
#226=CARTESIAN_POINT ( 'NONE',  ( 9.999999999999994671, 5.551115123125782702E-17, 8.000000000000058620 ) ) ;
#289=DIRECTION ( 'NONE',  ( 0.000000000000000000, -6.938893903907176763E-18, -1.000000000000000000 ) ) ;
#313=DIRECTION ( 'NONE',  ( -1.000000000000000000, 0.000000000000000000, 0.000000000000000000 ) ) ;
#316=ORIENTED_EDGE ( 'NONE', *, *, #15267, .F. ) ;
#371=AXIS2_PLACEMENT_3D ( 'NONE', #13826, #2695, #10622 ) ;
#378=DIRECTION ( 'NONE',  ( 0.000000000000000000, 0.8660254037844372643, -0.5000000000000024425 ) ) ;
#395=ORIENTED_EDGE ( 'NONE', *, *, #13776, .T. ) ;
#427=CARTESIAN_POINT ( 'NONE',  ( 1.500000000000001332, 0.000000000000000000, 0.000000000000000000 ) ) ;
#442=AXIS2_PLACEMENT_3D ( 'NONE', #5163, #8671, #19692 ) ;
#481=ADVANCED_FACE ( 'NONE', ( #18179 ), #19761, .F. ) ;
#504=VERTEX_POINT ( 'NONE', #19028 ) ;
#528=ORIENTED_EDGE ( 'NONE', *, *, #11637, .F. ) ;
#542=ORIENTED_EDGE ( 'NONE', *, *, #5514, .T. ) ;
#546=VECTOR ( 'NONE', #16332, 1000.000000000000114 ) ;
#657=ORIENTED_EDGE ( 'NONE', *, *, #13419, .T. ) ;
#677=CONICAL_SURFACE ( 'NONE', #12535, 4.057500000000029416, 1.047197551196593857 ) ;
#705=EDGE_LOOP ( 'NONE', ( #1909, #17255, #5302, #8140 ) ) ;
#758=ORIENTED_EDGE ( 'NONE', *, *, #19004, .F. ) ;
#828=DIRECTION ( 'NONE',  ( 0.000000000000000000, -6.938893903907177533E-18, -1.000000000000000000 ) ) ;
#842=LINE ( 'NONE', #15284, #12412 ) ;
#884=VERTEX_POINT ( 'NONE', #19733 ) ;
#951=VERTEX_POINT ( 'NONE', #2466 ) ;
#964=CARTESIAN_POINT ( 'NONE',  ( 5.000000000000004441, 4.685197434473814759, -6.938893903907228378E-15 ) ) ;
#989=DIRECTION ( 'NONE',  ( -1.000000000000000000, 0.000000000000000000, 0.000000000000000000 ) ) ;
#1003=( LENGTH_UNIT ( ) NAMED_UNIT ( * ) SI_UNIT ( .MILLI., .METRE. ) );
#1009=( LENGTH_UNIT ( ) NAMED_UNIT ( * ) SI_UNIT ( .MILLI., .METRE. ) );
#1024=EDGE_CURVE ( 'NONE', #3127, #14093, #15053, .T. ) ;
#1039=FACE_OUTER_BOUND ( 'NONE', #17212, .T. ) ;
#1072=CIRCLE ( 'NONE', #18666, 4.057500000000029416 ) ;
#1093=EDGE_CURVE ( 'NONE', #8938, #14630, #18997, .T. ) ;
#1113=AXIS2_PLACEMENT_3D ( 'NONE', #12855, #4784, #4680 ) ;
#1117=DIRECTION ( 'NONE',  ( 1.000000000000000000, 0.000000000000000000, 0.000000000000000000 ) ) ;
#1121=ADVANCED_FACE ( 'NONE', ( #11255 ), #18750, .T. ) ;
#1146=VERTEX_POINT ( 'NONE', #2883 ) ;
#1170=ORIENTED_EDGE ( 'NONE', *, *, #14358, .F. ) ;
#1179=DIRECTION ( 'NONE',  ( 0.000000000000000000, -0.4999999999999983902, 0.8660254037844394848 ) ) ;
#1180=FACE_OUTER_BOUND ( 'NONE', #11351, .T. ) ;
#1203=FACE_OUTER_BOUND ( 'NONE', #3532, .T. ) ;
#1210=EDGE_CURVE ( 'NONE', #884, #504, #2165, .T. ) ;
#1211=EDGE_CURVE ( 'NONE', #18631, #5527, #7743, .T. ) ;
#1224=VERTEX_POINT ( 'NONE', #14553 ) ;
#1255=ORIENTED_EDGE ( 'NONE', *, *, #14078, .T. ) ;
#1265=DIRECTION ( 'NONE',  ( -1.000000000000000000, 0.000000000000000000, 0.000000000000000000 ) ) ;
#1274=DIRECTION ( 'NONE',  ( 0.000000000000000000, 0.000000000000000000, 1.000000000000000000 ) ) ;
#1323=DIRECTION ( 'NONE',  ( 0.000000000000000000, -6.938893903907177533E-18, -1.000000000000000000 ) ) ;
#1354=CONICAL_SURFACE ( 'NONE', #14567, 4.172000000000029907, 0.7853981633974425058 ) ;
#1369=EDGE_LOOP ( 'NONE', ( #13585, #2991, #15137 ) ) ;
#1394=AXIS2_PLACEMENT_3D ( 'NONE', #12521, #7732, #16494 ) ;
#1397=VECTOR ( 'NONE', #12970, 1000.000000000000000 ) ;
#1400=DIRECTION ( 'NONE',  ( -0.000000000000000000, -1.000000000000000000, 1.117161918529055486E-15 ) ) ;
#1438=LINE ( 'NONE', #16173, #5723 ) ;
#1466=VERTEX_POINT ( 'NONE', #12416 ) ;
#1485=AXIS2_PLACEMENT_3D ( 'NONE', #4261, #10715, #2678 ) ;
#1572=LINE ( 'NONE', #4849, #18010 ) ;
#1573=CARTESIAN_POINT ( 'NONE',  ( 5.000000000000004441, 0.000000000000000000, 0.000000000000000000 ) ) ;
#1603=DIRECTION ( 'NONE',  ( -1.000000000000000000, 0.000000000000000000, 0.000000000000000000 ) ) ;
#1614=CARTESIAN_POINT ( 'NONE',  ( 5.000000000000004441, 7.027796151710827388, -4.057500000000009877 ) ) ;
#1715=ORIENTED_EDGE ( 'NONE', *, *, #13794, .T. ) ;
#1755=EDGE_CURVE ( 'NONE', #8267, #8276, #2281, .T. ) ;
#1784=DIRECTION ( 'NONE',  ( -1.000000000000000000, 0.000000000000000000, 0.000000000000000000 ) ) ;
#1800=DIRECTION ( 'NONE',  ( 0.000000000000000000, -0.8660254037844395958, -0.4999999999999984457 ) ) ;
#1821=CARTESIAN_POINT ( 'NONE',  ( 0.000000000000000000, 0.000000000000000000, 0.000000000000000000 ) ) ;
#1851=DIRECTION ( 'NONE',  ( 0.000000000000000000, -6.938893903907177533E-18, -1.000000000000000000 ) ) ;
#1857=CARTESIAN_POINT ( 'NONE',  ( 10.40000000000000568, 5.776289300541406836E-16, -5.000000000000000000 ) ) ;
#1874=DIRECTION ( 'NONE',  ( -0.000000000000000000, -1.000000000000000000, 1.117161918529055486E-15 ) ) ;
#1909=ORIENTED_EDGE ( 'NONE', *, *, #17823, .F. ) ;
#1945=CARTESIAN_POINT ( 'NONE',  ( 80.00000000000000000, 5.298012546456577047E-16, -4.171999999999999709 ) ) ;
#1954=CARTESIAN_POINT ( 'NONE',  ( 5.000000000000004441, 7.027796151710827388, -4.057500000000009877 ) ) ;
#1957=DIRECTION ( 'NONE',  ( 0.000000000000000000, 6.938893903907178303E-18, 1.000000000000000000 ) ) ;
#1993=DIRECTION ( 'NONE',  ( 0.000000000000000000, 1.000000000000000000, -1.302777330458572662E-15 ) ) ;
#2036=AXIS2_PLACEMENT_3D ( 'NONE', #19418, #6677, #13173 ) ;
#2107=EDGE_LOOP ( 'NONE', ( #8715, #203, #20384 ) ) ;
#2165=CIRCLE ( 'NONE', #5181, 8.000000000000058620 ) ;
#2235=ADVANCED_FACE ( 'NONE', ( #3526 ), #9968, .F. ) ;
#2281=LINE ( 'NONE', #5329, #17435 ) ;
#2287=APPLICATION_CONTEXT ( 'automotive_design' ) ;
#2333=CONICAL_SURFACE ( 'NONE', #19915, 4.057500000000029416, 1.047197551196593857 ) ;
#2421=DIRECTION ( 'NONE',  ( 1.000000000000000000, 0.000000000000000000, 0.000000000000000000 ) ) ;
#2450=CARTESIAN_POINT ( 'NONE',  ( 5.000000000000004441, -2.342598717236899830, 4.057500000000059615 ) ) ;
#2466=CARTESIAN_POINT ( 'NONE',  ( 0.000000000000000000, 4.510281037539699062E-17, 6.500000000000047962 ) ) ;
#2479=DIRECTION ( 'NONE',  ( 0.000000000000000000, 6.938893903907178303E-18, 1.000000000000000000 ) ) ;
#2506=EDGE_CURVE ( 'NONE', #17966, #10243, #16278, .T. ) ;
#2520=DIRECTION ( 'NONE',  ( -1.000000000000000000, 0.000000000000000000, 0.000000000000000000 ) ) ;
#2541=ORIENTED_EDGE ( 'NONE', *, *, #10632, .T. ) ;
#2555=CARTESIAN_POINT ( 'NONE',  ( 80.00000000000000000, 2.894906536710095477E-17, 4.172000000000029907 ) ) ;
#2600=AXIS2_PLACEMENT_3D ( 'NONE', #15052, #7168, #18524 ) ;
#2606=PRODUCT_DEFINITION_CONTEXT ( 'detailed design', #2972, 'design' ) ;
#2623=EDGE_LOOP ( 'NONE', ( #220, #18273, #8127, #4405, #15092 ) ) ;
#2678=DIRECTION ( 'NONE',  ( 0.000000000000000000, -6.938893903907167518E-18, -1.000000000000000000 ) ) ;
#2685=EDGE_CURVE ( 'NONE', #12506, #19519, #47, .T. ) ;
#2695=DIRECTION ( 'NONE',  ( 1.000000000000000000, 0.000000000000000000, 0.000000000000000000 ) ) ;
#2701=FACE_OUTER_BOUND ( 'NONE', #16340, .T. ) ;
#2706=FACE_OUTER_BOUND ( 'NONE', #10200, .T. ) ;
#2809=( NAMED_UNIT ( * ) PLANE_ANGLE_UNIT ( ) SI_UNIT ( $, .RADIAN. ) );
#2823=FACE_OUTER_BOUND ( 'NONE', #18288, .T. ) ;
#2857=CARTESIAN_POINT ( 'NONE',  ( -31.74999999999995737, 9.242062880866318385E-16, -8.000000000000058620 ) ) ;
#2881=CARTESIAN_POINT ( 'NONE',  ( 5.000000000000004441, -3.513898075855354630, 2.028750000000002274 ) ) ;
#2883=CARTESIAN_POINT ( 'NONE',  ( 9.999999999999998224, 6.987792986206746511E-16, 5.400000000000040323 ) ) ;
#2900=DIRECTION ( 'NONE',  ( 0.000000000000000000, 6.938893903907178303E-18, 1.000000000000000000 ) ) ;
#2972=APPLICATION_CONTEXT ( 'automotive_design' ) ;
#2985=AXIS2_PLACEMENT_3D ( 'NONE', #15650, #1117, #1323 ) ;
#2989=AXIS2_PLACEMENT_3D ( 'NONE', #4273, #20167, #12019 ) ;
#2991=ORIENTED_EDGE ( 'NONE', *, *, #15456, .F. ) ;
#3045=DIRECTION ( 'NONE',  ( -1.000000000000000000, 0.000000000000000000, 0.000000000000000000 ) ) ;
#3051=VERTEX_POINT ( 'NONE', #8409 ) ;
#3061=ADVANCED_FACE ( 'NONE', ( #6706 ), #5324, .F. ) ;
#3103=DIRECTION ( 'NONE',  ( 0.000000000000000000, 6.938893903907178303E-18, 1.000000000000000000 ) ) ;
#3120=VECTOR ( 'NONE', #7350, 1000.000000000000000 ) ;
#3127=VERTEX_POINT ( 'NONE', #1857 ) ;
#3228=CARTESIAN_POINT ( 'NONE',  ( -31.74999999999995737, 5.551115123125782702E-17, 8.000000000000058620 ) ) ;
#3258=MANIFOLD_SOLID_BREP ( 'Hex', #16440 ) ;
#3283=CARTESIAN_POINT ( 'NONE',  ( 5.000000000000004441, -2.342598717236899830, 4.057500000000059615 ) ) ;
#3398=AXIS2_PLACEMENT_3D ( 'NONE', #427, #313, #6759 ) ;
#3438=PLANE ( 'NONE',  #9216 ) ;
#3519=EDGE_CURVE ( 'NONE', #8913, #14068, #1438, .T. ) ;
#3526=FACE_OUTER_BOUND ( 'NONE', #11437, .T. ) ;
#3532=EDGE_LOOP ( 'NONE', ( #10982, #17084, #18296 ) ) ;
#3564=CARTESIAN_POINT ( 'NONE',  ( 5.000000000000004441, -2.342598717236899830, 4.057500000000059615 ) ) ;
#3580=DIRECTION ( 'NONE',  ( -1.000000000000000000, 0.000000000000000000, 0.000000000000000000 ) ) ;
#3625=CARTESIAN_POINT ( 'NONE',  ( 10.40000000000000568, 3.469446951953588921E-17, 5.000000000000000000 ) ) ;
#3639=ORIENTED_EDGE ( 'NONE', *, *, #11565, .F. ) ;
#3651=ADVANCED_FACE ( 'NONE', ( #2823 ), #677, .F. ) ;
#3673=ADVANCED_FACE ( 'NONE', ( #14903 ), #11807, .F. ) ;
#3695=ORIENTED_EDGE ( 'NONE', *, *, #11551, .T. ) ;
#3704=DIRECTION ( 'NONE',  ( 0.000000000000000000, -6.938893903907177533E-18, -1.000000000000000000 ) ) ;
#3729=VECTOR ( 'NONE', #12079, 1000.000000000000000 ) ;
#3789=AXIS2_PLACEMENT_3D ( 'NONE', #18321, #3894, #15269 ) ;
#3870=CARTESIAN_POINT ( 'NONE',  ( 5.000000000000004441, -4.685197434473809430, 6.071532165918824830E-15 ) ) ;
#3894=DIRECTION ( 'NONE',  ( 1.000000000000000000, 0.000000000000000000, 0.000000000000000000 ) ) ;
#3898=CARTESIAN_POINT ( 'NONE',  ( 0.000000000000000000, 2.342598717236856309, 4.057500000000020535 ) ) ;
#3930=EDGE_LOOP ( 'NONE', ( #10670, #19011, #15236, #8625, #528, #8180 ) ) ;
#3931=CIRCLE ( 'NONE', #4270, 5.000000000000035527 ) ;
#3991=ORIENTED_EDGE ( 'NONE', *, *, #7346, .T. ) ;
#4053=CARTESIAN_POINT ( 'NONE',  ( 5.000000000000004441, 0.000000000000000000, 0.000000000000000000 ) ) ;
#4060=EDGE_CURVE ( 'NONE', #884, #951, #4429, .T. ) ;
#4089=DIRECTION ( 'NONE',  ( -1.000000000000000000, 0.000000000000000000, 0.000000000000000000 ) ) ;
#4113=PLANE ( 'NONE',  #19394 ) ;
#4132=EDGE_CURVE ( 'NONE', #9807, #5527, #6674, .T. ) ;
#4190=AXIS2_PLACEMENT_3D ( 'NONE', #1614, #13165, #4892 ) ;
#4242=AXIS2_PLACEMENT_3D ( 'NONE', #18613, #4089, #16916 ) ;
#4247=LINE ( 'NONE', #17080, #8890 ) ;
#4261=CARTESIAN_POINT ( 'NONE',  ( 10.40000000000000568, -3.747002708109903570E-17, -5.400000000000040323 ) ) ;
#4270=AXIS2_PLACEMENT_3D ( 'NONE', #19694, #11655, #19585 ) ;
#4273=CARTESIAN_POINT ( 'NONE',  ( 9.999999999999994671, 0.000000000000000000, 0.000000000000000000 ) ) ;
#4287=ORIENTED_EDGE ( 'NONE', *, *, #7849, .T. ) ;
#4352=CARTESIAN_POINT ( 'NONE',  ( 5.000000000000004441, -4.685197434473809430, 6.071532165918824830E-15 ) ) ;
#4370=DIRECTION ( 'NONE',  ( 0.000000000000000000, -1.117161918529055683E-15, -1.000000000000000000 ) ) ;
#4404=ORIENTED_EDGE ( 'NONE', *, *, #5363, .F. ) ;
#4405=ORIENTED_EDGE ( 'NONE', *, *, #4132, .F. ) ;
#4429=CIRCLE ( 'NONE', #16965, 1.500000000000000444 ) ;
#4443=AXIS2_PLACEMENT_3D ( 'NONE', #13124, #8334, #289 ) ;
#4466=MECHANICAL_DESIGN_GEOMETRIC_PRESENTATION_REPRESENTATION('',(#7839),#20373);
#4483=EDGE_CURVE ( 'NONE', #8913, #8276, #19370, .T. ) ;
#4580=DIRECTION ( 'NONE',  ( 0.000000000000000000, 6.938893903907178303E-18, 1.000000000000000000 ) ) ;
#4606=ORIENTED_EDGE ( 'NONE', *, *, #19004, .T. ) ;
#4636=ADVANCED_FACE ( 'NONE', ( #17422 ), #1354, .T. ) ;
#4680=DIRECTION ( 'NONE',  ( 0.000000000000000000, 6.938893903907177533E-18, 1.000000000000000000 ) ) ;
#4683=CARTESIAN_POINT ( 'NONE',  ( -31.74999999999995737, 0.000000000000000000, 0.000000000000000000 ) ) ;
#4760=VECTOR ( 'NONE', #17997, 1000.000000000000114 ) ;
#4784=DIRECTION ( 'NONE',  ( -1.000000000000000000, 0.000000000000000000, 0.000000000000000000 ) ) ;
#4842=DIRECTION ( 'NONE',  ( -1.000000000000000000, 0.000000000000000000, 0.000000000000000000 ) ) ;
#4849=CARTESIAN_POINT ( 'NONE',  ( 5.000000000000004441, 2.342598717236856309, 4.057500000000020535 ) ) ;
#4857=EDGE_CURVE ( 'NONE', #14093, #1146, #17943, .T. ) ;
#4892=DIRECTION ( 'NONE',  ( 0.000000000000000000, -6.938893903907177533E-18, -1.000000000000000000 ) ) ;
#4893=FACE_BOUND ( 'NONE', #3930, .T. ) ;
#4913=DIRECTION ( 'NONE',  ( 0.000000000000000000, 6.938893903907178303E-18, 1.000000000000000000 ) ) ;
#4914=DIRECTION ( 'NONE',  ( 1.000000000000000000, 0.000000000000000000, 0.000000000000000000 ) ) ;
#4919=DIRECTION ( 'NONE',  ( 0.000000000000000000, -0.4999999999999982792, 0.8660254037844395958 ) ) ;
#4931=ORIENTED_EDGE ( 'NONE', *, *, #11637, .T. ) ;
#4933=DIRECTION ( 'NONE',  ( 0.000000000000000000, 6.938893903907178303E-18, 1.000000000000000000 ) ) ;
#4995=ORIENTED_EDGE ( 'NONE', *, *, #14078, .F. ) ;
#5058=CARTESIAN_POINT ( 'NONE',  ( 5.000000000000004441, 3.513898075855356407, -2.028750000000020481 ) ) ;
#5067=AXIS2_PLACEMENT_3D ( 'NONE', #1954, #9779, #14699 ) ;
#5071=FACE_OUTER_BOUND ( 'NONE', #16818, .T. ) ;
#5079=DIRECTION ( 'NONE',  ( -1.000000000000000000, 0.000000000000000000, 0.000000000000000000 ) ) ;
#5084=TOROIDAL_SURFACE ( 'NONE', #3398, 6.500000000000000888, 1.500000000000000000 ) ;
#5123=DIRECTION ( 'NONE',  ( 0.000000000000000000, 0.8660254037844395958, 0.4999999999999982792 ) ) ;
#5154=CARTESIAN_POINT ( 'NONE',  ( 9.999999999999994671, 0.000000000000000000, 0.000000000000000000 ) ) ;
#5163=CARTESIAN_POINT ( 'NONE',  ( -31.74999999999995737, 0.000000000000000000, 0.000000000000000000 ) ) ;
#5179=ORIENTED_EDGE ( 'NONE', *, *, #7076, .F. ) ;
#5180=ADVANCED_FACE ( 'NONE', ( #5071 ), #5084, .T. ) ;
#5181=AXIS2_PLACEMENT_3D ( 'NONE', #11039, #13055, #9430 ) ;
#5217=DIRECTION ( 'NONE',  ( -1.000000000000000000, 0.000000000000000000, 0.000000000000000000 ) ) ;
#5219=EDGE_CURVE ( 'NONE', #15362, #8267, #17812, .T. ) ;
#5282=VERTEX_POINT ( 'NONE', #18648 ) ;
#5289=LINE ( 'NONE', #14774, #16960 ) ;
#5302=ORIENTED_EDGE ( 'NONE', *, *, #1024, .T. ) ;
#5324=PLANE ( 'NONE',  #13946 ) ;
#5329=CARTESIAN_POINT ( 'NONE',  ( 5.000000000000004441, -4.685197434473809430, 6.071532165918824830E-15 ) ) ;
#5363=EDGE_CURVE ( 'NONE', #5282, #5621, #5587, .T. ) ;
#5365=FACE_OUTER_BOUND ( 'NONE', #2107, .T. ) ;
#5377=ORIENTED_EDGE ( 'NONE', *, *, #16011, .F. ) ;
#5425=ORIENTED_EDGE ( 'NONE', *, *, #5666, .T. ) ;
#5514=EDGE_CURVE ( 'NONE', #19519, #504, #17377, .T. ) ;
#5527=VERTEX_POINT ( 'NONE', #12820 ) ;
#5563=ORIENTED_EDGE ( 'NONE', *, *, #4857, .T. ) ;
#5583=ORIENTED_EDGE ( 'NONE', *, *, #18469, .T. ) ;
#5587=LINE ( 'NONE', #7088, #3729 ) ;
#5621=VERTEX_POINT ( 'NONE', #14527 ) ;
#5645=EDGE_CURVE ( 'NONE', #10243, #14630, #1072, .T. ) ;
#5666=EDGE_CURVE ( 'NONE', #1146, #14093, #12904, .T. ) ;
#5721=ORIENTED_EDGE ( 'NONE', *, *, #19864, .T. ) ;
#5723=VECTOR ( 'NONE', #7987, 1000.000000000000000 ) ;
#5734=ORIENTED_EDGE ( 'NONE', *, *, #218, .F. ) ;
#5851=CARTESIAN_POINT ( 'NONE',  ( 5.000000000000004441, 3.513898075855358183, 2.028750000000009379 ) ) ;
#5858=( NAMED_UNIT ( * ) SI_UNIT ( $, .STERADIAN. ) SOLID_ANGLE_UNIT ( ) );
#5918=CARTESIAN_POINT ( 'NONE',  ( 5.000000000000004441, 2.342598717236856309, 4.057500000000020535 ) ) ;
#5934=DIRECTION ( 'NONE',  ( -1.000000000000000000, 0.000000000000000000, 0.000000000000000000 ) ) ;
#5944=VECTOR ( 'NONE', #3045, 1000.000000000000000 ) ;
#5990=AXIS2_PLACEMENT_3D ( 'NONE', #18663, #7728, #18875 ) ;
#6005=VECTOR ( 'NONE', #19010, 1000.000000000000000 ) ;
#6032=CYLINDRICAL_SURFACE ( 'NONE', #1394, 8.000000000000058620 ) ;
#6091=LINE ( 'NONE', #9375, #17125 ) ;
#6189=AXIS2_PLACEMENT_3D ( 'NONE', #13765, #8877, #20427 ) ;
#6191=CARTESIAN_POINT ( 'NONE',  ( 0.000000000000000000, -4.685197434473809430, 6.071532165918824830E-15 ) ) ;
#6300=ADVANCED_FACE ( 'NONE', ( #4893, #6567 ), #9853, .T. ) ;
#6310=DIRECTION ( 'NONE',  ( -1.000000000000000000, 0.000000000000000000, 0.000000000000000000 ) ) ;
#6352=ORIENTED_EDGE ( 'NONE', *, *, #2506, .T. ) ;
#6368=DIRECTION ( 'NONE',  ( -1.000000000000000000, 0.000000000000000000, 0.000000000000000000 ) ) ;
#6406=ORIENTED_EDGE ( 'NONE', *, *, #9023, .F. ) ;
#6437=PLANE ( 'NONE',  #15504 ) ;
#6500=CARTESIAN_POINT ( 'NONE',  ( 5.000000000000004441, -4.685197434473809430, 6.071532165918824830E-15 ) ) ;
#6567=FACE_OUTER_BOUND ( 'NONE', #19026, .T. ) ;
#6577=ORIENTED_EDGE ( 'NONE', *, *, #15917, .F. ) ;
#6598=ADVANCED_FACE ( 'NONE', ( #1180 ), #6032, .T. ) ;
#6671=DIRECTION ( 'NONE',  ( -1.000000000000000000, 0.000000000000000000, 0.000000000000000000 ) ) ;
#6674=LINE ( 'NONE', #13169, #1397 ) ;
#6677=DIRECTION ( 'NONE',  ( -1.000000000000000000, -0.000000000000000000, -0.000000000000000000 ) ) ;
#6699=FACE_OUTER_BOUND ( 'NONE', #10330, .T. ) ;
#6706=FACE_OUTER_BOUND ( 'NONE', #8750, .T. ) ;
#6759=DIRECTION ( 'NONE',  ( 0.000000000000000000, 6.938893903907177533E-18, 1.000000000000000000 ) ) ;
#6772=CARTESIAN_POINT ( 'NONE',  ( 9.999999999999994671, 8.000000000000000000, 0.000000000000000000 ) ) ;
#6803=CARTESIAN_POINT ( 'NONE',  ( 5.000000000000004441, -3.469446951953614189E-15, -4.057500000000000107 ) ) ;
#7021=ORIENTED_EDGE ( 'NONE', *, *, #1210, .T. ) ;
#7065=ORIENTED_EDGE ( 'NONE', *, *, #1755, .F. ) ;
#7076=EDGE_CURVE ( 'NONE', #10243, #8938, #5289, .T. ) ;
#7088=CARTESIAN_POINT ( 'NONE',  ( 5.000000000000004441, -2.342598717236910044, -4.057499999999996554 ) ) ;
#7116=ORIENTED_EDGE ( 'NONE', *, *, #9528, .T. ) ;
#7137=CARTESIAN_POINT ( 'NONE',  ( 5.000000000000004441, 7.027796151710827388, -4.057500000000009877 ) ) ;
#7168=DIRECTION ( 'NONE',  ( 1.000000000000000000, 0.000000000000000000, 0.000000000000000000 ) ) ;
#7242=ORIENTED_EDGE ( 'NONE', *, *, #12591, .T. ) ;
#7261=ORIENTED_EDGE ( 'NONE', *, *, #2506, .F. ) ;
#7268=CARTESIAN_POINT ( 'NONE',  ( 5.000000000000004441, -2.342598717236899830, 4.057500000000059615 ) ) ;
#7290=DIRECTION ( 'NONE',  ( 0.000000000000000000, -0.5000000000000022204, -0.8660254037844372643 ) ) ;
#7326=DIRECTION ( 'NONE',  ( 0.000000000000000000, 1.000000000000000000, -1.117161918529055683E-15 ) ) ;
#7346=EDGE_CURVE ( 'NONE', #12709, #14678, #18528, .T. ) ;
#7350=DIRECTION ( 'NONE',  ( -0.000000000000000000, -1.000000000000000000, 1.117161918529055486E-15 ) ) ;
#7411=AXIS2_PLACEMENT_3D ( 'NONE', #13366, #5079, #10368 ) ;
#7444=ORIENTED_EDGE ( 'NONE', *, *, #14255, .F. ) ;
#7447=ADVANCED_FACE ( 'NONE', ( #17915 ), #6437, .T. ) ;
#7454=( NAMED_UNIT ( * ) PLANE_ANGLE_UNIT ( ) SI_UNIT ( $, .RADIAN. ) );
#7507=ORIENTED_EDGE ( 'NONE', *, *, #5219, .T. ) ;
#7539=CIRCLE ( 'NONE', #13305, 8.000000000000058620 ) ;
#7545=LINE ( 'NONE', #14038, #6005 ) ;
#7552=VECTOR ( 'NONE', #20474, 1000.000000000000000 ) ;
#7615=ORIENTED_EDGE ( 'NONE', *, *, #14555, .F. ) ;
#7631=VECTOR ( 'NONE', #1993, 1000.000000000000000 ) ;
#7648=CARTESIAN_POINT ( 'NONE',  ( 0.000000000000000000, 4.685197434473814759, -6.938893903907228378E-15 ) ) ;
#7665=ORIENTED_EDGE ( 'NONE', *, *, #14255, .T. ) ;
#7690=CARTESIAN_POINT ( 'NONE',  ( 5.000000000000004441, 0.000000000000000000, 0.000000000000000000 ) ) ;
#7728=DIRECTION ( 'NONE',  ( 1.000000000000000000, 0.000000000000000000, 0.000000000000000000 ) ) ;
#7732=DIRECTION ( 'NONE',  ( -1.000000000000000000, 0.000000000000000000, 0.000000000000000000 ) ) ;
#7743=LINE ( 'NONE', #16135, #17058 ) ;
#7762=ORIENTED_EDGE ( 'NONE', *, *, #5363, .T. ) ;
#7767=VECTOR ( 'NONE', #6310, 1000.000000000000000 ) ;
#7786=ORIENTED_EDGE ( 'NONE', *, *, #17691, .F. ) ;
#7805=LINE ( 'NONE', #14201, #5944 ) ;
#7839=STYLED_ITEM('',(#20995),#3258);
#7843=CARTESIAN_POINT ( 'NONE',  ( 5.000000000000004441, 0.000000000000000000, 0.000000000000000000 ) ) ;
#7849=EDGE_CURVE ( 'NONE', #8938, #20059, #15995, .T. ) ;
#7914=ORIENTED_EDGE ( 'NONE', *, *, #20504, .F. ) ;
#7943=TOROIDAL_SURFACE ( 'NONE', #17148, 5.400000000000000355, 0.4000000000000000222 ) ;
#7950=DIRECTION ( 'NONE',  ( 0.000000000000000000, 1.294035738186425244E-16, 1.000000000000000000 ) ) ;
#7987=DIRECTION ( 'NONE',  ( 0.000000000000000000, 1.000000000000000000, -1.302777330458572662E-15 ) ) ;
#8045=CARTESIAN_POINT ( 'NONE',  ( 5.000000000000004441, 2.342598717236899830, -4.057500000000030305 ) ) ;
#8127=ORIENTED_EDGE ( 'NONE', *, *, #27, .F. ) ;
#8140=ORIENTED_EDGE ( 'NONE', *, *, #5666, .F. ) ;
#8180=ORIENTED_EDGE ( 'NONE', *, *, #12536, .F. ) ;
#8217=ORIENTED_EDGE ( 'NONE', *, *, #2685, .T. ) ;
#8226=DIRECTION ( 'NONE',  ( 0.000000000000000000, 6.938893903907178303E-18, 1.000000000000000000 ) ) ;
#8250=LINE ( 'NONE', #19806, #546 ) ;
#8255=EDGE_LOOP ( 'NONE', ( #5563, #5425 ) ) ;
#8267=VERTEX_POINT ( 'NONE', #20722 ) ;
#8276=VERTEX_POINT ( 'NONE', #6191 ) ;
#8325=EDGE_LOOP ( 'NONE', ( #5734, #7116, #20844, #4995 ) ) ;
#8328=LINE ( 'NONE', #3564, #4760 ) ;
#8334=DIRECTION ( 'NONE',  ( -1.000000000000000000, -0.000000000000000000, -0.000000000000000000 ) ) ;
#8363=ADVANCED_FACE ( 'NONE', ( #6699 ), #19434, .F. ) ;
#8409=CARTESIAN_POINT ( 'NONE',  ( 0.000000000000000000, 8.375619485785039961E-16, -6.500000000000000888 ) ) ;
#8471=DIRECTION ( 'NONE',  ( -0.5000000000000006661, 1.000482654775420499E-16, -0.8660254037844382635 ) ) ;
#8554=LINE ( 'NONE', #8659, #11047 ) ;
#8566=CARTESIAN_POINT ( 'NONE',  ( 9.999999999999998224, -3.747002708109903570E-17, -5.400000000000040323 ) ) ;
#8570=ORIENTED_EDGE ( 'NONE', *, *, #18469, .F. ) ;
#8625=ORIENTED_EDGE ( 'NONE', *, *, #20750, .T. ) ;
#8659=CARTESIAN_POINT ( 'NONE',  ( -31.74999999999995737, 3.469446951953614189E-17, 5.000000000000036415 ) ) ;
#8671=DIRECTION ( 'NONE',  ( -1.000000000000000000, 0.000000000000000000, 0.000000000000000000 ) ) ;
#8715=ORIENTED_EDGE ( 'NONE', *, *, #14358, .T. ) ;
#8739=ORIENTED_EDGE ( 'NONE', *, *, #9528, .F. ) ;
#8741=ADVANCED_FACE ( 'NONE', ( #1203 ), #17209, .F. ) ;
#8750=EDGE_LOOP ( 'NONE', ( #13434, #16602, #8570 ) ) ;
#8762=DIRECTION ( 'NONE',  ( -1.000000000000000000, 0.000000000000000000, 0.000000000000000000 ) ) ;
#8775=CYLINDRICAL_SURFACE ( 'NONE', #6189, 8.000000000000058620 ) ;
#8791=ORIENTED_EDGE ( 'NONE', *, *, #20750, .F. ) ;
#8800=CARTESIAN_POINT ( 'NONE',  ( 1.500000000000001332, 0.000000000000000000, 0.000000000000000000 ) ) ;
#8859=VECTOR ( 'NONE', #8962, 1000.000000000000114 ) ;
#8877=DIRECTION ( 'NONE',  ( -1.000000000000000000, 0.000000000000000000, 0.000000000000000000 ) ) ;
#8890=VECTOR ( 'NONE', #20454, 1000.000000000000114 ) ;
#8913=VERTEX_POINT ( 'NONE', #20532 ) ;
#8938=VERTEX_POINT ( 'NONE', #19165 ) ;
#8962=DIRECTION ( 'NONE',  ( 0.000000000000000000, -0.4999999999999983902, 0.8660254037844394848 ) ) ;
#9023=EDGE_CURVE ( 'NONE', #9807, #8913, #19065, .T. ) ;
#9107=ORIENTED_EDGE ( 'NONE', *, *, #4060, .T. ) ;
#9126=EDGE_CURVE ( 'NONE', #9807, #15362, #8328, .T. ) ;
#9203=CARTESIAN_POINT ( 'NONE',  ( 7.342598717236928252, 0.000000000000000000, 0.000000000000000000 ) ) ;
#9216=AXIS2_PLACEMENT_3D ( 'NONE', #6500, #5123, #4919 ) ;
#9375=CARTESIAN_POINT ( 'NONE',  ( 80.00000000000000000, 4.819735792371784729E-16, -4.172000000000029907 ) ) ;
#9430=DIRECTION ( 'NONE',  ( 0.000000000000000000, 6.938893903907177533E-18, 1.000000000000000000 ) ) ;
#9487=EDGE_CURVE ( 'NONE', #12506, #884, #14491, .T. ) ;
#9502=AXIS2_PLACEMENT_3D ( 'NONE', #57, #9981, #1957 ) ;
#9528=EDGE_CURVE ( 'NONE', #14678, #12709, #18326, .T. ) ;
#9537=SHAPE_DEFINITION_REPRESENTATION ( #15013, #20602 ) ;
#9550=TOROIDAL_SURFACE ( 'NONE', #1113, 6.500000000000000888, 1.500000000000000000 ) ;
#9560=FACE_OUTER_BOUND ( 'NONE', #11678, .T. ) ;
#9577=CARTESIAN_POINT ( 'NONE',  ( 5.000000000000004441, 0.000000000000000000, 0.000000000000000000 ) ) ;
#9653=PLANE ( 'NONE',  #4190 ) ;
#9767=CIRCLE ( 'NONE', #7411, 4.057500000000029416 ) ;
#9779=DIRECTION ( 'NONE',  ( 1.000000000000000000, 0.000000000000000000, 0.000000000000000000 ) ) ;
#9801=CARTESIAN_POINT ( 'NONE',  ( 0.000000000000000000, 0.000000000000000000, 0.000000000000000000 ) ) ;
#9807=VERTEX_POINT ( 'NONE', #15743 ) ;
#9811=DIRECTION ( 'NONE',  ( -1.000000000000000000, 0.000000000000000000, 0.000000000000000000 ) ) ;
#9827=CYLINDRICAL_SURFACE ( 'NONE', #442, 5.000000000000036415 ) ;
#9850=ORIENTED_EDGE ( 'NONE', *, *, #7346, .F. ) ;
#9853=PLANE ( 'NONE',  #12251 ) ;
#9887=EDGE_LOOP ( 'NONE', ( #13393, #10878, #7261 ) ) ;
#9906=CARTESIAN_POINT ( 'NONE',  ( 5.000000000000004441, 2.342598717236899830, -4.057500000000030305 ) ) ;
#9930=AXIS2_PLACEMENT_3D ( 'NONE', #12956, #1603, #11350 ) ;
#9955=EDGE_CURVE ( 'NONE', #12709, #1466, #15299, .T. ) ;
#9968=PLANE ( 'NONE',  #19970 ) ;
#9981=DIRECTION ( 'NONE',  ( -1.000000000000000000, 0.000000000000000000, 0.000000000000000000 ) ) ;
#10018=ORIENTED_EDGE ( 'NONE', *, *, #15607, .F. ) ;
#10023=ORIENTED_EDGE ( 'NONE', *, *, #13292, .T. ) ;
#10030=CARTESIAN_POINT ( 'NONE',  ( 5.000000000000004441, 4.685197434473814759, -6.938893903907228378E-15 ) ) ;
#10122=VERTEX_POINT ( 'NONE', #5918 ) ;
#10200=EDGE_LOOP ( 'NONE', ( #6577, #20229, #19613, #14332 ) ) ;
#10201=ORIENTED_EDGE ( 'NONE', *, *, #218, .T. ) ;
#10243=VERTEX_POINT ( 'NONE', #5058 ) ;
#10248=AXIS2_PLACEMENT_3D ( 'NONE', #4683, #16049, #14775 ) ;
#10267=DIRECTION ( 'NONE',  ( 1.000000000000000000, 0.000000000000000000, 0.000000000000000000 ) ) ;
#10280=ORIENTED_EDGE ( 'NONE', *, *, #12591, .F. ) ;
#10330=EDGE_LOOP ( 'NONE', ( #16762, #87, #316 ) ) ;
#10368=DIRECTION ( 'NONE',  ( 0.000000000000000000, 6.938893903907178303E-18, 1.000000000000000000 ) ) ;
#10373=FACE_OUTER_BOUND ( 'NONE', #14777, .T. ) ;
#10491=ADVANCED_FACE ( 'NONE', ( #5365 ), #11966, .F. ) ;
#10508=AXIS2_PLACEMENT_3D ( 'NONE', #19209, #19306, #4580 ) ;
#10546=ORIENTED_EDGE ( 'NONE', *, *, #1755, .T. ) ;
#10591=PRODUCT ( 'socket head cap screw_iso_ISO 4762 M10 x 70 - 32N', 'socket head cap screw_iso_ISO 4762 M10 x 70 - 32N', '', ( #15926 ) ) ;
#10594=ADVANCED_BREP_SHAPE_REPRESENTATION ( '', ( #3258, #18233 ), #20586 ) ;
#10599=LINE ( 'NONE', #4352, #20434 ) ;
#10622=DIRECTION ( 'NONE',  ( 0.000000000000000000, -6.938893903907177533E-18, -1.000000000000000000 ) ) ;
#10632=EDGE_CURVE ( 'NONE', #951, #3051, #15340, .T. ) ;
#10638=ORIENTED_EDGE ( 'NONE', *, *, #1211, .F. ) ;
#10670=ORIENTED_EDGE ( 'NONE', *, *, #11565, .T. ) ;
#10694=FACE_OUTER_BOUND ( 'NONE', #2623, .T. ) ;
#10715=DIRECTION ( 'NONE',  ( 0.000000000000000000, -1.000000000000000000, 6.938893903907177533E-18 ) ) ;
#10743=CIRCLE ( 'NONE', #19546, 4.057500000000029416 ) ;
#10744=LINE ( 'NONE', #14278, #3120 ) ;
#10759=CIRCLE ( 'NONE', #20251, 0.4000000000000001887 ) ;
#10819=DIRECTION ( 'NONE',  ( 0.000000000000000000, 1.000000000000000000, 1.155257860108281416E-16 ) ) ;
#10869=EDGE_LOOP ( 'NONE', ( #14309, #4606, #5721, #5377 ) ) ;
#10878=ORIENTED_EDGE ( 'NONE', *, *, #15607, .T. ) ;
#10921=DIRECTION ( 'NONE',  ( -1.000000000000000000, 0.000000000000000000, 0.000000000000000000 ) ) ;
#10942=ADVANCED_FACE ( 'NONE', ( #17353 ), #3438, .T. ) ;
#10982=ORIENTED_EDGE ( 'NONE', *, *, #7076, .T. ) ;
#11039=CARTESIAN_POINT ( 'NONE',  ( 1.500000000000001332, 0.000000000000000000, 0.000000000000000000 ) ) ;
#11047=VECTOR ( 'NONE', #2520, 1000.000000000000000 ) ;
#11150=FACE_OUTER_BOUND ( 'NONE', #18116, .T. ) ;
#11181=ADVANCED_FACE ( 'NONE', ( #2701 ), #12243, .T. ) ;
#11212=ORIENTED_EDGE ( 'NONE', *, *, #20621, .T. ) ;
#11255=FACE_OUTER_BOUND ( 'NONE', #8325, .T. ) ;
#11335=CARTESIAN_POINT ( 'NONE',  ( 80.00000000000000000, 2.894906536710095477E-17, 4.172000000000029907 ) ) ;
#11350=DIRECTION ( 'NONE',  ( 0.000000000000000000, 6.938893903907178303E-18, 1.000000000000000000 ) ) ;
#11351=EDGE_LOOP ( 'NONE', ( #16004, #12299, #17786, #7021 ) ) ;
#11426=ORIENTED_EDGE ( 'NONE', *, *, #5645, .T. ) ;
#11437=EDGE_LOOP ( 'NONE', ( #4931, #4404, #1170, #16850, #4287 ) ) ;
#11475=UNCERTAINTY_MEASURE_WITH_UNIT (LENGTH_MEASURE( 1.000000000000000082E-05 ), #1003, 'distance_accuracy_value', 'NONE');
#11551=EDGE_CURVE ( 'NONE', #10122, #14068, #1572, .T. ) ;
#11565=EDGE_CURVE ( 'NONE', #12038, #14068, #16309, .T. ) ;
#11572=DIRECTION ( 'NONE',  ( 0.000000000000000000, 6.938893903907177533E-18, 1.000000000000000000 ) ) ;
#11637=EDGE_CURVE ( 'NONE', #20059, #5621, #10744, .T. ) ;
#11655=DIRECTION ( 'NONE',  ( -1.000000000000000000, 0.000000000000000000, 0.000000000000000000 ) ) ;
#11678=EDGE_LOOP ( 'NONE', ( #10638, #16307, #19094, #5583, #12989 ) ) ;
#11722=AXIS2_PLACEMENT_3D ( 'NONE', #18392, #378, #15233 ) ;
#11725=CIRCLE ( 'NONE', #2600, 5.000000000000036415 ) ;
#11733=LINE ( 'NONE', #9906, #12035 ) ;
#11781=DIRECTION ( 'NONE',  ( 0.000000000000000000, -0.5000000000000022204, -0.8660254037844372643 ) ) ;
#11790=CIRCLE ( 'NONE', #13476, 4.057500000000029416 ) ;
#11807=PLANE ( 'NONE',  #5067 ) ;
#11845=DIRECTION ( 'NONE',  ( 0.000000000000000000, 6.938893903907177533E-18, 1.000000000000000000 ) ) ;
#11966=PLANE ( 'NONE',  #3789 ) ;
#11992=DIRECTION ( 'NONE',  ( -0.7071067811865489050, 4.906538933386750403E-18, 0.7071067811865460184 ) ) ;
#12019=DIRECTION ( 'NONE',  ( 0.000000000000000000, 6.938893903907177533E-18, 1.000000000000000000 ) ) ;
#12035=VECTOR ( 'NONE', #1874, 1000.000000000000000 ) ;
#12038=VERTEX_POINT ( 'NONE', #7648 ) ;
#12079=DIRECTION ( 'NONE',  ( -1.000000000000000000, 0.000000000000000000, 0.000000000000000000 ) ) ;
#12164=LINE ( 'NONE', #7268, #7631 ) ;
#12231=VECTOR ( 'NONE', #19565, 1000.000000000000114 ) ;
#12243=PLANE ( 'NONE',  #12933 ) ;
#12246=ADVANCED_FACE ( 'NONE', ( #19211 ), #9550, .T. ) ;
#12251=AXIS2_PLACEMENT_3D ( 'NONE', #1821, #6671, #11572 ) ;
#12299=ORIENTED_EDGE ( 'NONE', *, *, #20504, .T. ) ;
#12332=DIRECTION ( 'NONE',  ( 0.000000000000000000, -1.155257860108280923E-16, 1.000000000000000000 ) ) ;
#12352=DIRECTION ( 'NONE',  ( 0.000000000000000000, 0.8660254037844375974, -0.5000000000000019984 ) ) ;
#12379=ADVANCED_FACE ( 'NONE', ( #19925, #10373 ), #16545, .T. ) ;
#12389=VECTOR ( 'NONE', #8471, 1000.000000000000114 ) ;
#12412=VECTOR ( 'NONE', #7290, 1000.000000000000114 ) ;
#12416=CARTESIAN_POINT ( 'NONE',  ( 79.17199999999999704, 3.469446951953613573E-17, 5.000000000000035527 ) ) ;
#12468=CARTESIAN_POINT ( 'NONE',  ( 0.000000000000000000, 2.342598717236899830, -4.057500000000030305 ) ) ;
#12506=VERTEX_POINT ( 'NONE', #226 ) ;
#12517=DIRECTION ( 'NONE',  ( 0.000000000000000000, 6.938893903907177533E-18, 1.000000000000000000 ) ) ;
#12521=CARTESIAN_POINT ( 'NONE',  ( -31.74999999999995737, 0.000000000000000000, 0.000000000000000000 ) ) ;
#12535=AXIS2_PLACEMENT_3D ( 'NONE', #9577, #16075, #4913 ) ;
#12536=EDGE_CURVE ( 'NONE', #12038, #20059, #4247, .T. ) ;
#12591=EDGE_CURVE ( 'NONE', #504, #884, #7539, .T. ) ;
#12663=CIRCLE ( 'NONE', #18737, 6.500000000000047962 ) ;
#12709=VERTEX_POINT ( 'NONE', #11335 ) ;
#12747=ADVANCED_FACE ( 'NONE', ( #19901 ), #9827, .T. ) ;
#12820=CARTESIAN_POINT ( 'NONE',  ( 5.000000000000004441, 6.938893903907228378E-15, 4.057500000000028528 ) ) ;
#12854=CARTESIAN_POINT ( 'NONE',  ( 9.999999999999994671, 9.242062880866249359E-16, -8.000000000000000000 ) ) ;
#12855=CARTESIAN_POINT ( 'NONE',  ( 1.500000000000001332, 0.000000000000000000, 0.000000000000000000 ) ) ;
#12904=CIRCLE ( 'NONE', #4443, 5.400000000000040323 ) ;
#12908=ADVANCED_FACE ( 'NONE', ( #1039 ), #8775, .T. ) ;
#12919=VECTOR ( 'NONE', #5217, 1000.000000000000000 ) ;
#12933=AXIS2_PLACEMENT_3D ( 'NONE', #14049, #12352, #15436 ) ;
#12956=CARTESIAN_POINT ( 'NONE',  ( 80.00000000000000000, 0.000000000000000000, 0.000000000000000000 ) ) ;
#12970=DIRECTION ( 'NONE',  ( 0.000000000000000000, 1.000000000000000000, -1.302777330458572662E-15 ) ) ;
#12989=ORIENTED_EDGE ( 'NONE', *, *, #15267, .T. ) ;
#13008=ADVANCED_FACE ( 'NONE', ( #16938 ), #4113, .T. ) ;
#13050=DIRECTION ( 'NONE',  ( 0.000000000000000000, -0.5000000000000018874, -0.8660254037844374864 ) ) ;
#13055=DIRECTION ( 'NONE',  ( 1.000000000000000000, -0.000000000000000000, -0.000000000000000000 ) ) ;
#13119=CARTESIAN_POINT ( 'NONE',  ( 0.000000000000000000, -2.342598717236899830, 4.057500000000059615 ) ) ;
#13124=CARTESIAN_POINT ( 'NONE',  ( 9.999999999999994671, 0.000000000000000000, 0.000000000000000000 ) ) ;
#13134=LINE ( 'NONE', #18110, #13199 ) ;
#13165=DIRECTION ( 'NONE',  ( 1.000000000000000000, 0.000000000000000000, 0.000000000000000000 ) ) ;
#13169=CARTESIAN_POINT ( 'NONE',  ( 5.000000000000004441, -2.342598717236899830, 4.057500000000059615 ) ) ;
#13173=DIRECTION ( 'NONE',  ( 0.000000000000000000, -6.938893903907176763E-18, -1.000000000000000000 ) ) ;
#13199=VECTOR ( 'NONE', #3580, 1000.000000000000000 ) ;
#13275=DIRECTION ( 'NONE',  ( 0.000000000000000000, -1.000000000000000000, 6.938893903907177533E-18 ) ) ;
#13292=EDGE_CURVE ( 'NONE', #19987, #5282, #18402, .T. ) ;
#13305=AXIS2_PLACEMENT_3D ( 'NONE', #8800, #16970, #12517 ) ;
#13366=CARTESIAN_POINT ( 'NONE',  ( 5.000000000000004441, 0.000000000000000000, 0.000000000000000000 ) ) ;
#13367=CARTESIAN_POINT ( 'NONE',  ( 5.000000000000004441, 4.687458767389385798E-16, -4.057500000000029416 ) ) ;
#13393=ORIENTED_EDGE ( 'NONE', *, *, #13794, .F. ) ;
#13419=EDGE_CURVE ( 'NONE', #3051, #951, #12663, .T. ) ;
#13434=ORIENTED_EDGE ( 'NONE', *, *, #13776, .F. ) ;
#13450=ADVANCED_FACE ( 'NONE', ( #11150 ), #16237, .T. ) ;
#13454=ORIENTED_EDGE ( 'NONE', *, *, #9955, .F. ) ;
#13476=AXIS2_PLACEMENT_3D ( 'NONE', #4053, #989, #2479 ) ;
#13532=ADVANCED_FACE ( 'NONE', ( #17938 ), #9653, .F. ) ;
#13585=ORIENTED_EDGE ( 'NONE', *, *, #27, .T. ) ;
#13765=CARTESIAN_POINT ( 'NONE',  ( -31.74999999999995737, 0.000000000000000000, 0.000000000000000000 ) ) ;
#13776=EDGE_CURVE ( 'NONE', #8267, #19987, #10599, .T. ) ;
#13792=AXIS2_PLACEMENT_3D ( 'NONE', #20767, #10921, #17393 ) ;
#13794=EDGE_CURVE ( 'NONE', #1224, #17966, #15507, .T. ) ;
#13825=CIRCLE ( 'NONE', #2989, 8.000000000000058620 ) ;
#13826=CARTESIAN_POINT ( 'NONE',  ( 5.000000000000004441, 7.027796151710827388, -4.057500000000009877 ) ) ;
#13946=AXIS2_PLACEMENT_3D ( 'NONE', #7137, #15125, #18495 ) ;
#13964=ORIENTED_EDGE ( 'NONE', *, *, #4483, .F. ) ;
#14026=VECTOR ( 'NONE', #1179, 1000.000000000000114 ) ;
#14038=CARTESIAN_POINT ( 'NONE',  ( 0.000000000000000000, -4.685197434473809430, 6.071532165918824830E-15 ) ) ;
#14049=CARTESIAN_POINT ( 'NONE',  ( 5.000000000000004441, -2.342598717236899830, 4.057500000000059615 ) ) ;
#14068=VERTEX_POINT ( 'NONE', #3898 ) ;
#14078=EDGE_CURVE ( 'NONE', #19163, #1466, #3931, .T. ) ;
#14093=VERTEX_POINT ( 'NONE', #8566 ) ;
#14201=CARTESIAN_POINT ( 'NONE',  ( 5.000000000000004441, 4.685197434473814759, -6.938893903907228378E-15 ) ) ;
#14226=DIRECTION ( 'NONE',  ( -0.000000000000000000, -1.000000000000000000, 1.302777330458572662E-15 ) ) ;
#14246=CARTESIAN_POINT ( 'NONE',  ( 1.500000000000001332, 7.509176090703883811E-16, -6.500000000000047962 ) ) ;
#14255=EDGE_CURVE ( 'NONE', #1224, #12038, #7805, .T. ) ;
#14272=VECTOR ( 'NONE', #13050, 1000.000000000000114 ) ;
#14278=CARTESIAN_POINT ( 'NONE',  ( 0.000000000000000000, 2.342598717236899830, -4.057500000000030305 ) ) ;
#14280=VECTOR ( 'NONE', #4842, 1000.000000000000000 ) ;
#14309=ORIENTED_EDGE ( 'NONE', *, *, #14555, .T. ) ;
#14332=ORIENTED_EDGE ( 'NONE', *, *, #1024, .F. ) ;
#14344=DIRECTION ( 'NONE',  ( 0.000000000000000000, 6.938893903907178303E-18, 1.000000000000000000 ) ) ;
#14358=EDGE_CURVE ( 'NONE', #14630, #5282, #11733, .T. ) ;
#14361=DIRECTION ( 'NONE',  ( -1.000000000000000000, 0.000000000000000000, 0.000000000000000000 ) ) ;
#14375=ADVANCED_FACE ( 'NONE', ( #14724 ), #7943, .F. ) ;
#14491=LINE ( 'NONE', #3228, #12919 ) ;
#14527=CARTESIAN_POINT ( 'NONE',  ( 0.000000000000000000, -2.342598717236910044, -4.057499999999996554 ) ) ;
#14545=ORIENTED_EDGE ( 'NONE', *, *, #16011, .T. ) ;
#14553=CARTESIAN_POINT ( 'NONE',  ( 5.000000000000004441, 4.685197434473814759, -6.938893903907228378E-15 ) ) ;
#14555=EDGE_CURVE ( 'NONE', #1466, #19163, #18842, .T. ) ;
#14567=AXIS2_PLACEMENT_3D ( 'NONE', #16056, #6368, #2900 ) ;
#14571=DIRECTION ( 'NONE',  ( 0.000000000000000000, 6.938893903907178303E-18, 1.000000000000000000 ) ) ;
#14593=AXIS2_PLACEMENT_3D ( 'NONE', #19538, #4914, #1851 ) ;
#14620=AXIS2_PLACEMENT_3D ( 'NONE', #5154, #8762, #11845 ) ;
#14630=VERTEX_POINT ( 'NONE', #6803 ) ;
#14678=VERTEX_POINT ( 'NONE', #1945 ) ;
#14699=DIRECTION ( 'NONE',  ( 0.000000000000000000, -6.938893903907177533E-18, -1.000000000000000000 ) ) ;
#14711=VECTOR ( 'NONE', #1400, 1000.000000000000000 ) ;
#14724=FACE_OUTER_BOUND ( 'NONE', #705, .T. ) ;
#14739=VERTEX_POINT ( 'NONE', #3625 ) ;
#14774=CARTESIAN_POINT ( 'NONE',  ( 5.000000000000004441, 4.685197434473814759, -6.938893903907228378E-15 ) ) ;
#14775=DIRECTION ( 'NONE',  ( 0.000000000000000000, 6.938893903907177533E-18, 1.000000000000000000 ) ) ;
#14777=EDGE_LOOP ( 'NONE', ( #16368, #7914 ) ) ;
#14903=FACE_OUTER_BOUND ( 'NONE', #1369, .T. ) ;
#14947=VECTOR ( 'NONE', #1265, 1000.000000000000000 ) ;
#14975=EDGE_CURVE ( 'NONE', #18631, #14630, #19814, .T. ) ;
#15013=PRODUCT_DEFINITION_SHAPE ( 'NONE', 'NONE',  #15369 ) ;
#15052=CARTESIAN_POINT ( 'NONE',  ( 10.40000000000000568, 0.000000000000000000, 0.000000000000000000 ) ) ;
#15053=CIRCLE ( 'NONE', #1485, 0.4000000000000001887 ) ;
#15092=ORIENTED_EDGE ( 'NONE', *, *, #9023, .T. ) ;
#15125=DIRECTION ( 'NONE',  ( 1.000000000000000000, 0.000000000000000000, 0.000000000000000000 ) ) ;
#15137=ORIENTED_EDGE ( 'NONE', *, *, #20621, .F. ) ;
#15233=DIRECTION ( 'NONE',  ( 0.000000000000000000, 0.5000000000000024425, 0.8660254037844372643 ) ) ;
#15236=ORIENTED_EDGE ( 'NONE', *, *, #4483, .T. ) ;
#15267=EDGE_CURVE ( 'NONE', #15362, #5527, #18493, .T. ) ;
#15269=DIRECTION ( 'NONE',  ( 0.000000000000000000, -6.938893903907177533E-18, -1.000000000000000000 ) ) ;
#15284=CARTESIAN_POINT ( 'NONE',  ( 5.000000000000004441, 4.685197434473814759, -6.938893903907228378E-15 ) ) ;
#15299=LINE ( 'NONE', #2555, #15324 ) ;
#15324=VECTOR ( 'NONE', #11992, 1000.000000000000114 ) ;
#15340=CIRCLE ( 'NONE', #17350, 6.500000000000047962 ) ;
#15362=VERTEX_POINT ( 'NONE', #2881 ) ;
#15369=PRODUCT_DEFINITION ( 'UNKNOWN', '', #16886, #2606 ) ;
#15436=DIRECTION ( 'NONE',  ( 0.000000000000000000, 0.5000000000000018874, 0.8660254037844374864 ) ) ;
#15443=SHAPE_REPRESENTATION_RELATIONSHIP ( 'NONE' , 'NONE' ,  #20602, #10594 ) ;
#15456=EDGE_CURVE ( 'NONE', #17966, #10122, #8250, .T. ) ;
#15504=AXIS2_PLACEMENT_3D ( 'NONE', #10030, #1800, #4 ) ;
#15507=LINE ( 'NONE', #964, #14026 ) ;
#15517=TOROIDAL_SURFACE ( 'NONE', #2985, 5.400000000000000355, 0.4000000000000000222 ) ;
#15607=EDGE_CURVE ( 'NONE', #1224, #10243, #842, .T. ) ;
#15650=CARTESIAN_POINT ( 'NONE',  ( 10.40000000000000568, 0.000000000000000000, 0.000000000000000000 ) ) ;
#15712=DIRECTION ( 'NONE',  ( 0.000000000000000000, 1.302777330458572662E-15, 1.000000000000000000 ) ) ;
#15743=CARTESIAN_POINT ( 'NONE',  ( 5.000000000000004441, -2.342598717236899830, 4.057500000000059615 ) ) ;
#15775=DIRECTION ( 'NONE',  ( -1.000000000000000000, 0.000000000000000000, 0.000000000000000000 ) ) ;
#15866=CIRCLE ( 'NONE', #17204, 1.500000000000000444 ) ;
#15871=DIRECTION ( 'NONE',  ( -0.7071067811865489050, 8.168906669016238096E-17, -0.7071067811865460184 ) ) ;
#15903=CARTESIAN_POINT ( 'NONE',  ( 0.000000000000000000, 0.000000000000000000, 0.000000000000000000 ) ) ;
#15917=EDGE_CURVE ( 'NONE', #14739, #3127, #11725, .T. ) ;
#15926=PRODUCT_CONTEXT ( 'NONE', #2287, 'mechanical' ) ;
#15948=CARTESIAN_POINT ( 'NONE',  ( 0.000000000000000000, 4.685197434473814759, -6.938893903907228378E-15 ) ) ;
#15995=LINE ( 'NONE', #20833, #7767 ) ;
#16004=ORIENTED_EDGE ( 'NONE', *, *, #5514, .F. ) ;
#16011=EDGE_CURVE ( 'NONE', #1466, #14739, #8554, .T. ) ;
#16049=DIRECTION ( 'NONE',  ( -1.000000000000000000, 0.000000000000000000, 0.000000000000000000 ) ) ;
#16056=CARTESIAN_POINT ( 'NONE',  ( 80.00000000000000000, 0.000000000000000000, 0.000000000000000000 ) ) ;
#16075=DIRECTION ( 'NONE',  ( -1.000000000000000000, 0.000000000000000000, 0.000000000000000000 ) ) ;
#16135=CARTESIAN_POINT ( 'NONE',  ( 5.000000000000004441, 2.815456201510357988E-17, 4.057500000000029416 ) ) ;
#16173=CARTESIAN_POINT ( 'NONE',  ( 0.000000000000000000, -2.342598717236899830, 4.057500000000059615 ) ) ;
#16237=CYLINDRICAL_SURFACE ( 'NONE', #10248, 5.000000000000036415 ) ;
#16257=EDGE_LOOP ( 'NONE', ( #3991, #10201, #7615, #13454 ) ) ;
#16278=CIRCLE ( 'NONE', #10508, 4.057500000000029416 ) ;
#16301=ORIENTED_EDGE ( 'NONE', *, *, #15456, .T. ) ;
#16307=ORIENTED_EDGE ( 'NONE', *, *, #14975, .T. ) ;
#16309=LINE ( 'NONE', #15948, #8859 ) ;
#16323=CARTESIAN_POINT ( 'NONE',  ( 5.000000000000004441, -3.513898075855361736, -2.028750000000006715 ) ) ;
#16332=DIRECTION ( 'NONE',  ( 0.000000000000000000, -0.4999999999999983902, 0.8660254037844394848 ) ) ;
#16340=EDGE_LOOP ( 'NONE', ( #13964, #6406, #17779, #7507, #10546 ) ) ;
#16368=ORIENTED_EDGE ( 'NONE', *, *, #2685, .F. ) ;
#16440=CLOSED_SHELL ( 'NONE', ( #18071, #12246, #17454, #4636, #12747, #12908, #6300, #6598, #12379, #13450, #1121, #13008, #14375, #5180, #7447, #19894, #11181, #10942, #2235, #481, #10491, #3061, #8363, #3673, #13532, #8741, #3651 ) ) ;
#16462=CARTESIAN_POINT ( 'NONE',  ( 5.000000000000004441, 2.342598717236899830, -4.057500000000030305 ) ) ;
#16494=DIRECTION ( 'NONE',  ( 0.000000000000000000, 6.938893903907177533E-18, 1.000000000000000000 ) ) ;
#16545=PLANE ( 'NONE',  #19383 ) ;
#16602=ORIENTED_EDGE ( 'NONE', *, *, #5219, .F. ) ;
#16762=ORIENTED_EDGE ( 'NONE', *, *, #9126, .F. ) ;
#16818=EDGE_LOOP ( 'NONE', ( #7786, #19143, #9107, #18304 ) ) ;
#16841=ORIENTED_EDGE ( 'NONE', *, *, #10632, .F. ) ;
#16850=ORIENTED_EDGE ( 'NONE', *, *, #1093, .F. ) ;
#16886=PRODUCT_DEFINITION_FORMATION_WITH_SPECIFIED_SOURCE ( 'ANY', '', #10591, .NOT_KNOWN. ) ;
#16916=DIRECTION ( 'NONE',  ( 0.000000000000000000, 6.938893903907177533E-18, 1.000000000000000000 ) ) ;
#16938=FACE_OUTER_BOUND ( 'NONE', #19739, .T. ) ;
#16960=VECTOR ( 'NONE', #11781, 1000.000000000000114 ) ;
#16965=AXIS2_PLACEMENT_3D ( 'NONE', #19826, #13275, #19614 ) ;
#16970=DIRECTION ( 'NONE',  ( 1.000000000000000000, -0.000000000000000000, -0.000000000000000000 ) ) ;
#16986=ORIENTED_EDGE ( 'NONE', *, *, #9487, .F. ) ;
#17058=VECTOR ( 'NONE', #19102, 1000.000000000000114 ) ;
#17070=ORIENTED_EDGE ( 'NONE', *, *, #14975, .F. ) ;
#17080=CARTESIAN_POINT ( 'NONE',  ( 0.000000000000000000, 4.685197434473814759, -6.938893903907228378E-15 ) ) ;
#17084=ORIENTED_EDGE ( 'NONE', *, *, #1093, .T. ) ;
#17125=VECTOR ( 'NONE', #15871, 1000.000000000000114 ) ;
#17148=AXIS2_PLACEMENT_3D ( 'NONE', #18295, #176, #18092 ) ;
#17204=AXIS2_PLACEMENT_3D ( 'NONE', #14246, #10819, #12332 ) ;
#17209=PLANE ( 'NONE',  #371 ) ;
#17212=EDGE_LOOP ( 'NONE', ( #8217, #542, #7242, #16986 ) ) ;
#17251=CARTESIAN_POINT ( 'NONE',  ( 80.00000000000000000, 4.172000000000002373, -2.710505431213761085E-17 ) ) ;
#17255=ORIENTED_EDGE ( 'NONE', *, *, #19864, .F. ) ;
#17273=EDGE_LOOP ( 'NONE', ( #10280, #19672, #16841, #17852 ) ) ;
#17329=EDGE_CURVE ( 'NONE', #14630, #19987, #10743, .T. ) ;
#17350=AXIS2_PLACEMENT_3D ( 'NONE', #9801, #20934, #4933 ) ;
#17353=FACE_OUTER_BOUND ( 'NONE', #20943, .T. ) ;
#17377=LINE ( 'NONE', #2857, #14947 ) ;
#17381=EDGE_LOOP ( 'NONE', ( #3639, #7444, #1715, #16301, #3695 ) ) ;
#17393=DIRECTION ( 'NONE',  ( 0.000000000000000000, 6.938893903907178303E-18, 1.000000000000000000 ) ) ;
#17422=FACE_OUTER_BOUND ( 'NONE', #16257, .T. ) ;
#17435=VECTOR ( 'NONE', #19968, 1000.000000000000000 ) ;
#17454=ADVANCED_FACE ( 'NONE', ( #2706 ), #15517, .F. ) ;
#17618=DIRECTION ( 'NONE',  ( 0.000000000000000000, 1.000000000000000000, -1.294035738186424998E-16 ) ) ;
#17635=CARTESIAN_POINT ( 'NONE',  ( 5.000000000000004441, 0.000000000000000000, 0.000000000000000000 ) ) ;
#17691=EDGE_CURVE ( 'NONE', #504, #3051, #15866, .T. ) ;
#17779=ORIENTED_EDGE ( 'NONE', *, *, #9126, .T. ) ;
#17786=ORIENTED_EDGE ( 'NONE', *, *, #9487, .T. ) ;
#17812=LINE ( 'NONE', #3283, #14272 ) ;
#17823=EDGE_CURVE ( 'NONE', #14739, #1146, #10759, .T. ) ;
#17852=ORIENTED_EDGE ( 'NONE', *, *, #4060, .F. ) ;
#17915=FACE_OUTER_BOUND ( 'NONE', #17381, .T. ) ;
#17938=FACE_OUTER_BOUND ( 'NONE', #9887, .T. ) ;
#17943=CIRCLE ( 'NONE', #2036, 5.400000000000040323 ) ;
#17966=VERTEX_POINT ( 'NONE', #5851 ) ;
#17997=DIRECTION ( 'NONE',  ( 0.000000000000000000, -0.5000000000000018874, -0.8660254037844374864 ) ) ;
#18010=VECTOR ( 'NONE', #9811, 1000.000000000000000 ) ;
#18071=ADVANCED_FACE ( 'NONE', ( #9560 ), #2333, .F. ) ;
#18092=DIRECTION ( 'NONE',  ( 0.000000000000000000, -6.938893903907177533E-18, -1.000000000000000000 ) ) ;
#18110=CARTESIAN_POINT ( 'NONE',  ( -31.74999999999995737, 5.776289300541449237E-16, -5.000000000000036415 ) ) ;
#18116=EDGE_LOOP ( 'NONE', ( #758, #1255, #14545, #18933 ) ) ;
#18179=FACE_OUTER_BOUND ( 'NONE', #19347, .T. ) ;
#18233=AXIS2_PLACEMENT_3D ( 'NONE', #15903, #1274, #19656 ) ;
#18273=ORIENTED_EDGE ( 'NONE', *, *, #11551, .F. ) ;
#18288=EDGE_LOOP ( 'NONE', ( #17070, #18376, #11212, #6352, #11426 ) ) ;
#18295=CARTESIAN_POINT ( 'NONE',  ( 10.40000000000000568, 0.000000000000000000, 0.000000000000000000 ) ) ;
#18296=ORIENTED_EDGE ( 'NONE', *, *, #5645, .F. ) ;
#18304=ORIENTED_EDGE ( 'NONE', *, *, #13419, .F. ) ;
#18321=CARTESIAN_POINT ( 'NONE',  ( 5.000000000000004441, 7.027796151710827388, -4.057500000000009877 ) ) ;
#18326=CIRCLE ( 'NONE', #9502, 4.172000000000029907 ) ;
#18376=ORIENTED_EDGE ( 'NONE', *, *, #1211, .T. ) ;
#18392=CARTESIAN_POINT ( 'NONE',  ( 5.000000000000004441, 4.685197434473814759, -6.938893903907228378E-15 ) ) ;
#18402=LINE ( 'NONE', #3870, #7552 ) ;
#18469=EDGE_CURVE ( 'NONE', #19987, #15362, #9767, .T. ) ;
#18493=CIRCLE ( 'NONE', #18826, 4.057500000000029416 ) ;
#18495=DIRECTION ( 'NONE',  ( 0.000000000000000000, -6.938893903907177533E-18, -1.000000000000000000 ) ) ;
#18524=DIRECTION ( 'NONE',  ( 0.000000000000000000, -6.938893903907177533E-18, -1.000000000000000000 ) ) ;
#18528=CIRCLE ( 'NONE', #13792, 4.172000000000029907 ) ;
#18613=CARTESIAN_POINT ( 'NONE',  ( 79.17199999999999704, 0.000000000000000000, 0.000000000000000000 ) ) ;
#18631=VERTEX_POINT ( 'NONE', #9203 ) ;
#18648=CARTESIAN_POINT ( 'NONE',  ( 5.000000000000004441, -2.342598717236910044, -4.057499999999996554 ) ) ;
#18663=CARTESIAN_POINT ( 'NONE',  ( 10.40000000000000568, 0.000000000000000000, 0.000000000000000000 ) ) ;
#18666=AXIS2_PLACEMENT_3D ( 'NONE', #1573, #1784, #8226 ) ;
#18737=AXIS2_PLACEMENT_3D ( 'NONE', #19311, #14361, #3103 ) ;
#18750=CONICAL_SURFACE ( 'NONE', #9930, 4.172000000000029907, 0.7853981633974425058 ) ;
#18814=( NAMED_UNIT ( * ) SI_UNIT ( $, .STERADIAN. ) SOLID_ANGLE_UNIT ( ) );
#18826=AXIS2_PLACEMENT_3D ( 'NONE', #7843, #5934, #14344 ) ;
#18842=CIRCLE ( 'NONE', #4242, 5.000000000000035527 ) ;
#18875=DIRECTION ( 'NONE',  ( 0.000000000000000000, -6.938893903907177533E-18, -1.000000000000000000 ) ) ;
#18878=CIRCLE ( 'NONE', #5990, 5.000000000000036415 ) ;
#18933=ORIENTED_EDGE ( 'NONE', *, *, #15917, .T. ) ;
#18940=DIRECTION ( 'NONE',  ( 0.000000000000000000, 6.938893903907178303E-18, 1.000000000000000000 ) ) ;
#18997=LINE ( 'NONE', #8045, #14711 ) ;
#19004=EDGE_CURVE ( 'NONE', #19163, #3127, #13134, .T. ) ;
#19010=DIRECTION ( 'NONE',  ( 0.000000000000000000, 0.4999999999999983347, -0.8660254037844395958 ) ) ;
#19011=ORIENTED_EDGE ( 'NONE', *, *, #3519, .F. ) ;
#19026=EDGE_LOOP ( 'NONE', ( #2541, #657 ) ) ;
#19028=CARTESIAN_POINT ( 'NONE',  ( 1.500000000000001332, 9.242062880866249359E-16, -8.000000000000000000 ) ) ;
#19063=ORIENTED_EDGE ( 'NONE', *, *, #12536, .T. ) ;
#19065=LINE ( 'NONE', #182, #14280 ) ;
#19094=ORIENTED_EDGE ( 'NONE', *, *, #17329, .T. ) ;
#19102=DIRECTION ( 'NONE',  ( -0.5000000000000006661, 6.009258394948590704E-18, 0.8660254037844382635 ) ) ;
#19122=DIRECTION ( 'NONE',  ( -1.000000000000000000, 0.000000000000000000, 0.000000000000000000 ) ) ;
#19143=ORIENTED_EDGE ( 'NONE', *, *, #1210, .F. ) ;
#19163=VERTEX_POINT ( 'NONE', #20930 ) ;
#19165=CARTESIAN_POINT ( 'NONE',  ( 5.000000000000004441, 2.342598717236899830, -4.057500000000030305 ) ) ;
#19209=CARTESIAN_POINT ( 'NONE',  ( 5.000000000000004441, 0.000000000000000000, 0.000000000000000000 ) ) ;
#19211=FACE_OUTER_BOUND ( 'NONE', #17273, .T. ) ;
#19306=DIRECTION ( 'NONE',  ( -1.000000000000000000, 0.000000000000000000, 0.000000000000000000 ) ) ;
#19311=CARTESIAN_POINT ( 'NONE',  ( 0.000000000000000000, 0.000000000000000000, 0.000000000000000000 ) ) ;
#19347=EDGE_LOOP ( 'NONE', ( #19063, #19541, #5179, #10018, #7665 ) ) ;
#19370=LINE ( 'NONE', #13119, #12231 ) ;
#19383=AXIS2_PLACEMENT_3D ( 'NONE', #6772, #10267, #3704 ) ;
#19394=AXIS2_PLACEMENT_3D ( 'NONE', #17251, #2421, #828 ) ;
#19418=CARTESIAN_POINT ( 'NONE',  ( 9.999999999999994671, 0.000000000000000000, 0.000000000000000000 ) ) ;
#19434=PLANE ( 'NONE',  #14593 ) ;
#19519=VERTEX_POINT ( 'NONE', #12854 ) ;
#19538=CARTESIAN_POINT ( 'NONE',  ( 5.000000000000004441, 7.027796151710827388, -4.057500000000009877 ) ) ;
#19541=ORIENTED_EDGE ( 'NONE', *, *, #7849, .F. ) ;
#19546=AXIS2_PLACEMENT_3D ( 'NONE', #7690, #15775, #18940 ) ;
#19565=DIRECTION ( 'NONE',  ( 0.000000000000000000, -0.5000000000000018874, -0.8660254037844374864 ) ) ;
#19585=DIRECTION ( 'NONE',  ( 0.000000000000000000, 6.938893903907177533E-18, 1.000000000000000000 ) ) ;
#19613=ORIENTED_EDGE ( 'NONE', *, *, #4857, .F. ) ;
#19614=DIRECTION ( 'NONE',  ( 0.000000000000000000, -6.938893903907175992E-18, -1.000000000000000000 ) ) ;
#19656=DIRECTION ( 'NONE',  ( 1.000000000000000000, 0.000000000000000000, 0.000000000000000000 ) ) ;
#19672=ORIENTED_EDGE ( 'NONE', *, *, #17691, .T. ) ;
#19692=DIRECTION ( 'NONE',  ( 0.000000000000000000, 6.938893903907177533E-18, 1.000000000000000000 ) ) ;
#19694=CARTESIAN_POINT ( 'NONE',  ( 79.17199999999999704, 0.000000000000000000, 0.000000000000000000 ) ) ;
#19733=CARTESIAN_POINT ( 'NONE',  ( 1.500000000000001332, 5.551115123125782702E-17, 8.000000000000058620 ) ) ;
#19739=EDGE_LOOP ( 'NONE', ( #9850, #8739 ) ) ;
#19761=PLANE ( 'NONE',  #11722 ) ;
#19806=CARTESIAN_POINT ( 'NONE',  ( 5.000000000000004441, 4.685197434473814759, -6.938893903907228378E-15 ) ) ;
#19814=LINE ( 'NONE', #13367, #12389 ) ;
#19826=CARTESIAN_POINT ( 'NONE',  ( 1.500000000000001332, 4.510281037539699062E-17, 6.500000000000047962 ) ) ;
#19864=EDGE_CURVE ( 'NONE', #3127, #14739, #18878, .T. ) ;
#19894=ADVANCED_FACE ( 'NONE', ( #10694 ), #20655, .F. ) ;
#19901=FACE_OUTER_BOUND ( 'NONE', #10869, .T. ) ;
#19915=AXIS2_PLACEMENT_3D ( 'NONE', #17635, #19122, #14571 ) ;
#19925=FACE_BOUND ( 'NONE', #8255, .T. ) ;
#19968=DIRECTION ( 'NONE',  ( -1.000000000000000000, 0.000000000000000000, 0.000000000000000000 ) ) ;
#19970=AXIS2_PLACEMENT_3D ( 'NONE', #16462, #4370, #7326 ) ;
#19987=VERTEX_POINT ( 'NONE', #16323 ) ;
#20059=VERTEX_POINT ( 'NONE', #12468 ) ;
#20167=DIRECTION ( 'NONE',  ( -1.000000000000000000, 0.000000000000000000, 0.000000000000000000 ) ) ;
#20229=ORIENTED_EDGE ( 'NONE', *, *, #17823, .T. ) ;
#20251=AXIS2_PLACEMENT_3D ( 'NONE', #20877, #17618, #7950 ) ;
#20373=( GEOMETRIC_REPRESENTATION_CONTEXT ( 3 ) GLOBAL_UNCERTAINTY_ASSIGNED_CONTEXT ( ( #11475 ) ) GLOBAL_UNIT_ASSIGNED_CONTEXT ( ( #1003, #2809, #5858 ) ) REPRESENTATION_CONTEXT ( 'NONE', 'WORKASPACE' ) );
#20384=ORIENTED_EDGE ( 'NONE', *, *, #17329, .F. ) ;
#20427=DIRECTION ( 'NONE',  ( 0.000000000000000000, 6.938893903907177533E-18, 1.000000000000000000 ) ) ;
#20434=VECTOR ( 'NONE', #20559, 1000.000000000000000 ) ;
#20454=DIRECTION ( 'NONE',  ( 0.000000000000000000, -0.5000000000000022204, -0.8660254037844372643 ) ) ;
#20474=DIRECTION ( 'NONE',  ( 0.000000000000000000, 0.4999999999999983347, -0.8660254037844395958 ) ) ;
#20504=EDGE_CURVE ( 'NONE', #19519, #12506, #13825, .T. ) ;
#20532=CARTESIAN_POINT ( 'NONE',  ( 0.000000000000000000, -2.342598717236899830, 4.057500000000059615 ) ) ;
#20557=AXIS2_PLACEMENT_3D ( 'NONE', #2450, #15712, #14226 ) ;
#20559=DIRECTION ( 'NONE',  ( 0.000000000000000000, 0.4999999999999983347, -0.8660254037844395958 ) ) ;
#20586=( GEOMETRIC_REPRESENTATION_CONTEXT ( 3 ) GLOBAL_UNCERTAINTY_ASSIGNED_CONTEXT ( ( #20595 ) ) GLOBAL_UNIT_ASSIGNED_CONTEXT ( ( #1009, #7454, #18814 ) ) REPRESENTATION_CONTEXT ( 'NONE', 'WORKASPACE' ) );
#20595=UNCERTAINTY_MEASURE_WITH_UNIT (LENGTH_MEASURE( 1.000000000000000082E-05 ), #1009, 'distance_accuracy_value', 'NONE');
#20602=SHAPE_REPRESENTATION ( 'socket head cap screw_iso_ISO 4762 M10 x 70 - 32N', ( #18233 ), #20586 ) ;
#20621=EDGE_CURVE ( 'NONE', #5527, #17966, #11790, .T. ) ;
#20655=PLANE ( 'NONE',  #20557 ) ;
#20722=CARTESIAN_POINT ( 'NONE',  ( 5.000000000000004441, -4.685197434473809430, 6.071532165918824830E-15 ) ) ;
#20750=EDGE_CURVE ( 'NONE', #8276, #5621, #7545, .T. ) ;
#20767=CARTESIAN_POINT ( 'NONE',  ( 80.00000000000000000, 0.000000000000000000, 0.000000000000000000 ) ) ;
#20833=CARTESIAN_POINT ( 'NONE',  ( 5.000000000000004441, 2.342598717236899830, -4.057500000000030305 ) ) ;
#20844=ORIENTED_EDGE ( 'NONE', *, *, #9955, .T. ) ;
#20877=CARTESIAN_POINT ( 'NONE',  ( 10.40000000000000568, 6.987792986206746511E-16, 5.400000000000040323 ) ) ;
#20930=CARTESIAN_POINT ( 'NONE',  ( 79.17199999999999704, 5.776289300541406836E-16, -4.999999999999999112 ) ) ;
#20934=DIRECTION ( 'NONE',  ( -1.000000000000000000, 0.000000000000000000, 0.000000000000000000 ) ) ;
#20943=EDGE_LOOP ( 'NONE', ( #8791, #7065, #395, #10023, #7762 ) ) ;
#20989=COLOUR_RGB('Black',0.12,0.14,0.17);
#20990=FILL_AREA_STYLE_COLOUR('',#20989);
#20991=FILL_AREA_STYLE('',(#20990));
#20992=SURFACE_STYLE_FILL_AREA(#20991);
#20993=SURFACE_SIDE_STYLE('',(#20992));
#20994=SURFACE_STYLE_USAGE(.BOTH.,#20993);
#20995=PRESENTATION_STYLE_ASSIGNMENT((#20994));
ENDSEC;
END-ISO-10303-21;
